ISO-10303-21;
HEADER;
/* Generated by software containing ST-Developer
 * from STEP Tools, Inc. (www.steptools.com) 
 */

FILE_DESCRIPTION(
/* description */ ('STEP AP214'),
/* implementation_level */ '2;1');

FILE_NAME(
/* name */ 'Axle Bolt.step',
/* time_stamp */ '2026-11-14T06:16:09-08:00',
/* author */ (''),
/* organization */ (''),
/* preprocessor_version */ 'ST-DEVELOPER v20.2',
/* originating_system */ 'Autodesk Translation Framework v15.17.0.0',
/* authorisation */ '');

FILE_SCHEMA (('AUTOMOTIVE_DESIGN { 1 0 10303 214 3 1 1 }'));
ENDSEC;

DATA;
#10=MECHANICAL_DESIGN_GEOMETRIC_PRESENTATION_REPRESENTATION('',(#354),#18006);
#95=(
BOUNDED_CURVE()
B_SPLINE_CURVE(2,(#17284,#17285,#17286),.UNSPECIFIED.,.F.,.F.)
B_SPLINE_CURVE_WITH_KNOTS((3,3),(-2.0333659945968,-1.31472121783515),
 .UNSPECIFIED.)
CURVE()
GEOMETRIC_REPRESENTATION_ITEM()
RATIONAL_B_SPLINE_CURVE((2.35176643423756,2.35176643423756,2.18291720111281))
REPRESENTATION_ITEM('')
);
#96=(
BOUNDED_CURVE()
B_SPLINE_CURVE(2,(#17288,#17289,#17290),.UNSPECIFIED.,.F.,.F.)
B_SPLINE_CURVE_WITH_KNOTS((3,3),(-2.75201077135845,-2.0333659945968),
 .UNSPECIFIED.)
CURVE()
GEOMETRIC_REPRESENTATION_ITEM()
RATIONAL_B_SPLINE_CURVE((2.18291720111281,2.35176643423756,2.35176643423756))
REPRESENTATION_ITEM('')
);
#97=(
BOUNDED_CURVE()
B_SPLINE_CURVE(2,(#17304,#17305,#17306),.UNSPECIFIED.,.F.,.F.)
B_SPLINE_CURVE_WITH_KNOTS((3,3),(-2.0333659945968,-1.31472121783515),
 .UNSPECIFIED.)
CURVE()
GEOMETRIC_REPRESENTATION_ITEM()
RATIONAL_B_SPLINE_CURVE((2.35176643423756,2.35176643423756,2.18291720111281))
REPRESENTATION_ITEM('')
);
#98=(
BOUNDED_CURVE()
B_SPLINE_CURVE(2,(#17307,#17308,#17309),.UNSPECIFIED.,.F.,.F.)
B_SPLINE_CURVE_WITH_KNOTS((3,3),(-2.75201077135845,-2.0333659945968),
 .UNSPECIFIED.)
CURVE()
GEOMETRIC_REPRESENTATION_ITEM()
RATIONAL_B_SPLINE_CURVE((2.18291720111281,2.35176643423756,2.35176643423756))
REPRESENTATION_ITEM('')
);
#99=(
BOUNDED_CURVE()
B_SPLINE_CURVE(2,(#17312,#17313,#17314),.UNSPECIFIED.,.F.,.F.)
B_SPLINE_CURVE_WITH_KNOTS((3,3),(-2.0333659945968,-1.31472121783515),
 .UNSPECIFIED.)
CURVE()
GEOMETRIC_REPRESENTATION_ITEM()
RATIONAL_B_SPLINE_CURVE((2.35176643423756,2.35176643423756,2.18291720111281))
REPRESENTATION_ITEM('')
);
#100=(
BOUNDED_CURVE()
B_SPLINE_CURVE(2,(#17315,#17316,#17317),.UNSPECIFIED.,.F.,.F.)
B_SPLINE_CURVE_WITH_KNOTS((3,3),(-2.75201077135844,-2.03336599459679),
 .UNSPECIFIED.)
CURVE()
GEOMETRIC_REPRESENTATION_ITEM()
RATIONAL_B_SPLINE_CURVE((2.18291720111281,2.35176643423757,2.35176643423757))
REPRESENTATION_ITEM('')
);
#101=(
BOUNDED_CURVE()
B_SPLINE_CURVE(2,(#17320,#17321,#17322),.UNSPECIFIED.,.F.,.F.)
B_SPLINE_CURVE_WITH_KNOTS((3,3),(-2.03336599459679,-1.31472121783515),
 .UNSPECIFIED.)
CURVE()
GEOMETRIC_REPRESENTATION_ITEM()
RATIONAL_B_SPLINE_CURVE((2.35176643423756,2.35176643423756,2.18291720111281))
REPRESENTATION_ITEM('')
);
#102=(
BOUNDED_CURVE()
B_SPLINE_CURVE(2,(#17323,#17324,#17325),.UNSPECIFIED.,.F.,.F.)
B_SPLINE_CURVE_WITH_KNOTS((3,3),(-2.75201077135844,-2.0333659945968),
 .UNSPECIFIED.)
CURVE()
GEOMETRIC_REPRESENTATION_ITEM()
RATIONAL_B_SPLINE_CURVE((2.18291720111281,2.35176643423756,2.35176643423756))
REPRESENTATION_ITEM('')
);
#103=(
BOUNDED_CURVE()
B_SPLINE_CURVE(2,(#17328,#17329,#17330),.UNSPECIFIED.,.F.,.F.)
B_SPLINE_CURVE_WITH_KNOTS((3,3),(-2.0333659945968,-1.31472121783515),
 .UNSPECIFIED.)
CURVE()
GEOMETRIC_REPRESENTATION_ITEM()
RATIONAL_B_SPLINE_CURVE((2.35176643423756,2.35176643423756,2.18291720111281))
REPRESENTATION_ITEM('')
);
#104=(
BOUNDED_CURVE()
B_SPLINE_CURVE(2,(#17331,#17332,#17333),.UNSPECIFIED.,.F.,.F.)
B_SPLINE_CURVE_WITH_KNOTS((3,3),(-2.75201077135844,-2.03336599459679),
 .UNSPECIFIED.)
CURVE()
GEOMETRIC_REPRESENTATION_ITEM()
RATIONAL_B_SPLINE_CURVE((2.18291720111281,2.35176643423757,2.35176643423757))
REPRESENTATION_ITEM('')
);
#105=(
BOUNDED_CURVE()
B_SPLINE_CURVE(2,(#17336,#17337,#17338),.UNSPECIFIED.,.F.,.F.)
B_SPLINE_CURVE_WITH_KNOTS((3,3),(-2.03336599459679,-1.31472121783515),
 .UNSPECIFIED.)
CURVE()
GEOMETRIC_REPRESENTATION_ITEM()
RATIONAL_B_SPLINE_CURVE((2.35176643423756,2.35176643423756,2.18291720111281))
REPRESENTATION_ITEM('')
);
#106=(
BOUNDED_CURVE()
B_SPLINE_CURVE(2,(#17339,#17340,#17341),.UNSPECIFIED.,.F.,.F.)
B_SPLINE_CURVE_WITH_KNOTS((3,3),(-2.75201077135844,-2.0333659945968),
 .UNSPECIFIED.)
CURVE()
GEOMETRIC_REPRESENTATION_ITEM()
RATIONAL_B_SPLINE_CURVE((2.18291720111281,2.35176643423756,2.35176643423756))
REPRESENTATION_ITEM('')
);
#119=CONICAL_SURFACE('',#10522,3.175,0.785398163397445);
#120=CONICAL_SURFACE('',#10524,5.588,1.30899693899575);
#121=CONICAL_SURFACE('',#10532,5.588,1.30899693899575);
#122=CONICAL_SURFACE('',#10533,5.588,1.30899693899575);
#123=CONICAL_SURFACE('',#10534,5.588,1.30899693899575);
#124=CONICAL_SURFACE('',#10535,5.588,1.30899693899575);
#125=CONICAL_SURFACE('',#10536,5.588,1.30899693899575);
#239=TOROIDAL_SURFACE('',#10509,4.4323,0.508);
#240=TOROIDAL_SURFACE('',#10515,3.4163,0.507999999999992);
#322=SHAPE_REPRESENTATION_RELATIONSHIP('SRR','None',#18080,#338);
#338=ADVANCED_BREP_SHAPE_REPRESENTATION('',(#370),#17997);
#354=STYLED_ITEM('',(#18171),#370);
#370=MANIFOLD_SOLID_BREP('Body1',#9563);
#469=FACE_BOUND('',#1952,.T.);
#470=FACE_BOUND('',#1954,.T.);
#776=PLANE('',#10526);
#777=PLANE('',#10537);
#778=PLANE('',#10538);
#779=PLANE('',#10539);
#780=PLANE('',#10540);
#781=PLANE('',#10541);
#782=PLANE('',#10542);
#783=PLANE('',#10543);
#784=PLANE('',#10544);
#785=PLANE('',#10545);
#1266=FACE_OUTER_BOUND('',#1932,.T.);
#1267=FACE_OUTER_BOUND('',#1933,.T.);
#1268=FACE_OUTER_BOUND('',#1934,.T.);
#1269=FACE_OUTER_BOUND('',#1935,.T.);
#1270=FACE_OUTER_BOUND('',#1936,.T.);
#1271=FACE_OUTER_BOUND('',#1937,.T.);
#1272=FACE_OUTER_BOUND('',#1938,.T.);
#1273=FACE_OUTER_BOUND('',#1939,.T.);
#1274=FACE_OUTER_BOUND('',#1940,.T.);
#1275=FACE_OUTER_BOUND('',#1941,.T.);
#1276=FACE_OUTER_BOUND('',#1942,.T.);
#1277=FACE_OUTER_BOUND('',#1943,.T.);
#1278=FACE_OUTER_BOUND('',#1944,.T.);
#1279=FACE_OUTER_BOUND('',#1945,.T.);
#1280=FACE_OUTER_BOUND('',#1946,.T.);
#1281=FACE_OUTER_BOUND('',#1947,.T.);
#1282=FACE_OUTER_BOUND('',#1948,.T.);
#1283=FACE_OUTER_BOUND('',#1949,.T.);
#1284=FACE_OUTER_BOUND('',#1950,.T.);
#1285=FACE_OUTER_BOUND('',#1951,.T.);
#1286=FACE_OUTER_BOUND('',#1953,.T.);
#1932=EDGE_LOOP('',(#8210,#8211,#8212,#8213));
#1933=EDGE_LOOP('',(#8214,#8215,#8216,#8217));
#1934=EDGE_LOOP('',(#8218,#8219,#8220,#8221));
#1935=EDGE_LOOP('',(#8222,#8223,#8224,#8225,#8226));
#1936=EDGE_LOOP('',(#8227,#8228,#8229,#8230,#8231));
#1937=EDGE_LOOP('',(#8232,#8233,#8234));
#1938=EDGE_LOOP('',(#8235,#8236,#8237,#8238,#8239,#8240));
#1939=EDGE_LOOP('',(#8241,#8242,#8243));
#1940=EDGE_LOOP('',(#8244,#8245,#8246));
#1941=EDGE_LOOP('',(#8247,#8248,#8249));
#1942=EDGE_LOOP('',(#8250,#8251,#8252));
#1943=EDGE_LOOP('',(#8253,#8254,#8255));
#1944=EDGE_LOOP('',(#8256,#8257,#8258,#8259,#8260));
#1945=EDGE_LOOP('',(#8261,#8262,#8263,#8264,#8265));
#1946=EDGE_LOOP('',(#8266,#8267,#8268,#8269,#8270));
#1947=EDGE_LOOP('',(#8271,#8272,#8273,#8274,#8275));
#1948=EDGE_LOOP('',(#8276,#8277,#8278,#8279,#8280));
#1949=EDGE_LOOP('',(#8281,#8282,#8283,#8284,#8285));
#1950=EDGE_LOOP('',(#8286));
#1951=EDGE_LOOP('',(#8287));
#1952=EDGE_LOOP('',(#8288));
#1953=EDGE_LOOP('',(#8289,#8290,#8291,#8292,#8293,#8294));
#1954=EDGE_LOOP('',(#8295));
#2737=LINE('',#17264,#3461);
#2738=LINE('',#17275,#3462);
#2739=LINE('',#17279,#3463);
#2740=LINE('',#17344,#3464);
#2741=LINE('',#17346,#3465);
#2742=LINE('',#17347,#3466);
#2743=LINE('',#17350,#3467);
#2744=LINE('',#17351,#3468);
#2745=LINE('',#17354,#3469);
#2746=LINE('',#17355,#3470);
#2747=LINE('',#17358,#3471);
#2748=LINE('',#17359,#3472);
#2749=LINE('',#17362,#3473);
#2750=LINE('',#17363,#3474);
#2751=LINE('',#17365,#3475);
#3461=VECTOR('',#13014,3.9243);
#3462=VECTOR('',#13027,3.175);
#3463=VECTOR('',#13032,3.175);
#3464=VECTOR('',#13063,1000.);
#3465=VECTOR('',#13064,1000.);
#3466=VECTOR('',#13065,1000.);
#3467=VECTOR('',#13068,1000.);
#3468=VECTOR('',#13069,1000.);
#3469=VECTOR('',#13072,1000.);
#3470=VECTOR('',#13073,1000.);
#3471=VECTOR('',#13076,1000.);
#3472=VECTOR('',#13077,1000.);
#3473=VECTOR('',#13080,1000.);
#3474=VECTOR('',#13081,1000.);
#3475=VECTOR('',#13084,1000.);
#3841=CIRCLE('',#10510,3.9243);
#3842=CIRCLE('',#10511,0.508);
#3843=CIRCLE('',#10512,4.4323);
#3844=CIRCLE('',#10514,3.9243);
#3845=CIRCLE('',#10516,3.4163);
#3846=CIRCLE('',#10517,0.507999999999992);
#3847=CIRCLE('',#10519,3.175);
#3848=CIRCLE('',#10520,3.175);
#3849=CIRCLE('',#10521,3.175);
#3850=CIRCLE('',#10523,2.1844);
#3851=CIRCLE('',#10525,5.588);
#3852=CIRCLE('',#10527,5.588);
#3853=CIRCLE('',#10528,5.588);
#3854=CIRCLE('',#10529,5.588);
#3855=CIRCLE('',#10530,5.588);
#3856=CIRCLE('',#10531,5.588);
#4639=VERTEX_POINT('',#17256);
#4640=VERTEX_POINT('',#17258);
#4641=VERTEX_POINT('',#17262);
#4642=VERTEX_POINT('',#17266);
#4643=VERTEX_POINT('',#17270);
#4644=VERTEX_POINT('',#17271);
#4645=VERTEX_POINT('',#17274);
#4646=VERTEX_POINT('',#17278);
#4647=VERTEX_POINT('',#17282);
#4648=VERTEX_POINT('',#17283);
#4649=VERTEX_POINT('',#17287);
#4650=VERTEX_POINT('',#17293);
#4651=VERTEX_POINT('',#17294);
#4652=VERTEX_POINT('',#17296);
#4653=VERTEX_POINT('',#17299);
#4654=VERTEX_POINT('',#17303);
#4655=VERTEX_POINT('',#17311);
#4656=VERTEX_POINT('',#17319);
#4657=VERTEX_POINT('',#17327);
#4658=VERTEX_POINT('',#17335);
#4659=VERTEX_POINT('',#17343);
#4660=VERTEX_POINT('',#17345);
#4661=VERTEX_POINT('',#17349);
#4662=VERTEX_POINT('',#17353);
#4663=VERTEX_POINT('',#17357);
#4664=VERTEX_POINT('',#17361);
#5853=EDGE_CURVE('',#4639,#4639,#3841,.T.);
#5854=EDGE_CURVE('',#4639,#4640,#3842,.T.);
#5855=EDGE_CURVE('',#4640,#4640,#3843,.T.);
#5856=EDGE_CURVE('',#4641,#4641,#3844,.T.);
#5857=EDGE_CURVE('',#4641,#4639,#2737,.T.);
#5858=EDGE_CURVE('',#4642,#4642,#3845,.T.);
#5859=EDGE_CURVE('',#4642,#4641,#3846,.T.);
#5860=EDGE_CURVE('',#4643,#4644,#3847,.T.);
#5861=EDGE_CURVE('',#4644,#4643,#3848,.T.);
#5862=EDGE_CURVE('',#4644,#4645,#2738,.T.);
#5863=EDGE_CURVE('',#4645,#4645,#3849,.T.);
#5864=EDGE_CURVE('',#4643,#4646,#2739,.T.);
#5865=EDGE_CURVE('',#4646,#4646,#3850,.T.);
#5866=EDGE_CURVE('',#4647,#4648,#95,.T.);
#5867=EDGE_CURVE('',#4648,#4649,#96,.T.);
#5868=EDGE_CURVE('',#4649,#4647,#3851,.T.);
#5869=EDGE_CURVE('',#4650,#4651,#3852,.T.);
#5870=EDGE_CURVE('',#4652,#4650,#3853,.T.);
#5871=EDGE_CURVE('',#4647,#4652,#3854,.T.);
#5872=EDGE_CURVE('',#4653,#4649,#3855,.T.);
#5873=EDGE_CURVE('',#4651,#4653,#3856,.T.);
#5874=EDGE_CURVE('',#4651,#4654,#97,.T.);
#5875=EDGE_CURVE('',#4654,#4650,#98,.T.);
#5876=EDGE_CURVE('',#4650,#4655,#99,.T.);
#5877=EDGE_CURVE('',#4655,#4652,#100,.T.);
#5878=EDGE_CURVE('',#4652,#4656,#101,.T.);
#5879=EDGE_CURVE('',#4656,#4647,#102,.T.);
#5880=EDGE_CURVE('',#4649,#4657,#103,.T.);
#5881=EDGE_CURVE('',#4657,#4653,#104,.T.);
#5882=EDGE_CURVE('',#4653,#4658,#105,.T.);
#5883=EDGE_CURVE('',#4658,#4651,#106,.T.);
#5884=EDGE_CURVE('',#4659,#4656,#2740,.T.);
#5885=EDGE_CURVE('',#4660,#4659,#2741,.T.);
#5886=EDGE_CURVE('',#4660,#4648,#2742,.T.);
#5887=EDGE_CURVE('',#4661,#4655,#2743,.T.);
#5888=EDGE_CURVE('',#4659,#4661,#2744,.T.);
#5889=EDGE_CURVE('',#4662,#4654,#2745,.T.);
#5890=EDGE_CURVE('',#4661,#4662,#2746,.T.);
#5891=EDGE_CURVE('',#4663,#4658,#2747,.T.);
#5892=EDGE_CURVE('',#4662,#4663,#2748,.T.);
#5893=EDGE_CURVE('',#4664,#4657,#2749,.T.);
#5894=EDGE_CURVE('',#4663,#4664,#2750,.T.);
#5895=EDGE_CURVE('',#4664,#4660,#2751,.T.);
#8210=ORIENTED_EDGE('',*,*,#5853,.F.);
#8211=ORIENTED_EDGE('',*,*,#5854,.T.);
#8212=ORIENTED_EDGE('',*,*,#5855,.T.);
#8213=ORIENTED_EDGE('',*,*,#5854,.F.);
#8214=ORIENTED_EDGE('',*,*,#5856,.F.);
#8215=ORIENTED_EDGE('',*,*,#5857,.T.);
#8216=ORIENTED_EDGE('',*,*,#5853,.T.);
#8217=ORIENTED_EDGE('',*,*,#5857,.F.);
#8218=ORIENTED_EDGE('',*,*,#5858,.F.);
#8219=ORIENTED_EDGE('',*,*,#5859,.T.);
#8220=ORIENTED_EDGE('',*,*,#5856,.T.);
#8221=ORIENTED_EDGE('',*,*,#5859,.F.);
#8222=ORIENTED_EDGE('',*,*,#5860,.F.);
#8223=ORIENTED_EDGE('',*,*,#5861,.F.);
#8224=ORIENTED_EDGE('',*,*,#5862,.T.);
#8225=ORIENTED_EDGE('',*,*,#5863,.T.);
#8226=ORIENTED_EDGE('',*,*,#5862,.F.);
#8227=ORIENTED_EDGE('',*,*,#5860,.T.);
#8228=ORIENTED_EDGE('',*,*,#5861,.T.);
#8229=ORIENTED_EDGE('',*,*,#5864,.T.);
#8230=ORIENTED_EDGE('',*,*,#5865,.F.);
#8231=ORIENTED_EDGE('',*,*,#5864,.F.);
#8232=ORIENTED_EDGE('',*,*,#5866,.T.);
#8233=ORIENTED_EDGE('',*,*,#5867,.T.);
#8234=ORIENTED_EDGE('',*,*,#5868,.T.);
#8235=ORIENTED_EDGE('',*,*,#5869,.F.);
#8236=ORIENTED_EDGE('',*,*,#5870,.F.);
#8237=ORIENTED_EDGE('',*,*,#5871,.F.);
#8238=ORIENTED_EDGE('',*,*,#5868,.F.);
#8239=ORIENTED_EDGE('',*,*,#5872,.F.);
#8240=ORIENTED_EDGE('',*,*,#5873,.F.);
#8241=ORIENTED_EDGE('',*,*,#5869,.T.);
#8242=ORIENTED_EDGE('',*,*,#5874,.T.);
#8243=ORIENTED_EDGE('',*,*,#5875,.T.);
#8244=ORIENTED_EDGE('',*,*,#5870,.T.);
#8245=ORIENTED_EDGE('',*,*,#5876,.T.);
#8246=ORIENTED_EDGE('',*,*,#5877,.T.);
#8247=ORIENTED_EDGE('',*,*,#5871,.T.);
#8248=ORIENTED_EDGE('',*,*,#5878,.T.);
#8249=ORIENTED_EDGE('',*,*,#5879,.T.);
#8250=ORIENTED_EDGE('',*,*,#5872,.T.);
#8251=ORIENTED_EDGE('',*,*,#5880,.T.);
#8252=ORIENTED_EDGE('',*,*,#5881,.T.);
#8253=ORIENTED_EDGE('',*,*,#5873,.T.);
#8254=ORIENTED_EDGE('',*,*,#5882,.T.);
#8255=ORIENTED_EDGE('',*,*,#5883,.T.);
#8256=ORIENTED_EDGE('',*,*,#5884,.F.);
#8257=ORIENTED_EDGE('',*,*,#5885,.F.);
#8258=ORIENTED_EDGE('',*,*,#5886,.T.);
#8259=ORIENTED_EDGE('',*,*,#5866,.F.);
#8260=ORIENTED_EDGE('',*,*,#5879,.F.);
#8261=ORIENTED_EDGE('',*,*,#5887,.F.);
#8262=ORIENTED_EDGE('',*,*,#5888,.F.);
#8263=ORIENTED_EDGE('',*,*,#5884,.T.);
#8264=ORIENTED_EDGE('',*,*,#5878,.F.);
#8265=ORIENTED_EDGE('',*,*,#5877,.F.);
#8266=ORIENTED_EDGE('',*,*,#5889,.F.);
#8267=ORIENTED_EDGE('',*,*,#5890,.F.);
#8268=ORIENTED_EDGE('',*,*,#5887,.T.);
#8269=ORIENTED_EDGE('',*,*,#5876,.F.);
#8270=ORIENTED_EDGE('',*,*,#5875,.F.);
#8271=ORIENTED_EDGE('',*,*,#5891,.F.);
#8272=ORIENTED_EDGE('',*,*,#5892,.F.);
#8273=ORIENTED_EDGE('',*,*,#5889,.T.);
#8274=ORIENTED_EDGE('',*,*,#5874,.F.);
#8275=ORIENTED_EDGE('',*,*,#5883,.F.);
#8276=ORIENTED_EDGE('',*,*,#5893,.F.);
#8277=ORIENTED_EDGE('',*,*,#5894,.F.);
#8278=ORIENTED_EDGE('',*,*,#5891,.T.);
#8279=ORIENTED_EDGE('',*,*,#5882,.F.);
#8280=ORIENTED_EDGE('',*,*,#5881,.F.);
#8281=ORIENTED_EDGE('',*,*,#5886,.F.);
#8282=ORIENTED_EDGE('',*,*,#5895,.F.);
#8283=ORIENTED_EDGE('',*,*,#5893,.T.);
#8284=ORIENTED_EDGE('',*,*,#5880,.F.);
#8285=ORIENTED_EDGE('',*,*,#5867,.F.);
#8286=ORIENTED_EDGE('',*,*,#5865,.T.);
#8287=ORIENTED_EDGE('',*,*,#5858,.T.);
#8288=ORIENTED_EDGE('',*,*,#5863,.F.);
#8289=ORIENTED_EDGE('',*,*,#5894,.T.);
#8290=ORIENTED_EDGE('',*,*,#5895,.T.);
#8291=ORIENTED_EDGE('',*,*,#5885,.T.);
#8292=ORIENTED_EDGE('',*,*,#5888,.T.);
#8293=ORIENTED_EDGE('',*,*,#5890,.T.);
#8294=ORIENTED_EDGE('',*,*,#5892,.T.);
#8295=ORIENTED_EDGE('',*,*,#5855,.F.);
#8957=CYLINDRICAL_SURFACE('',#10513,3.9243);
#8958=CYLINDRICAL_SURFACE('',#10518,3.175);
#9405=ADVANCED_FACE('',(#1266),#239,.F.);
#9406=ADVANCED_FACE('',(#1267),#8957,.T.);
#9407=ADVANCED_FACE('',(#1268),#240,.T.);
#9408=ADVANCED_FACE('',(#1269),#8958,.T.);
#9409=ADVANCED_FACE('',(#1270),#119,.T.);
#9410=ADVANCED_FACE('',(#1271),#120,.T.);
#9411=ADVANCED_FACE('',(#1272),#776,.F.);
#9412=ADVANCED_FACE('',(#1273),#121,.T.);
#9413=ADVANCED_FACE('',(#1274),#122,.T.);
#9414=ADVANCED_FACE('',(#1275),#123,.T.);
#9415=ADVANCED_FACE('',(#1276),#124,.T.);
#9416=ADVANCED_FACE('',(#1277),#125,.T.);
#9417=ADVANCED_FACE('',(#1278),#777,.F.);
#9418=ADVANCED_FACE('',(#1279),#778,.F.);
#9419=ADVANCED_FACE('',(#1280),#779,.F.);
#9420=ADVANCED_FACE('',(#1281),#780,.F.);
#9421=ADVANCED_FACE('',(#1282),#781,.F.);
#9422=ADVANCED_FACE('',(#1283),#782,.F.);
#9423=ADVANCED_FACE('',(#1284),#783,.F.);
#9424=ADVANCED_FACE('',(#1285,#469),#784,.F.);
#9425=ADVANCED_FACE('',(#1286,#470),#785,.F.);
#9563=CLOSED_SHELL('',(#9405,#9406,#9407,#9408,#9409,#9410,#9411,#9412,
#9413,#9414,#9415,#9416,#9417,#9418,#9419,#9420,#9421,#9422,#9423,#9424,
#9425));
#10508=AXIS2_PLACEMENT_3D('',#17254,#13000,#13001);
#10509=AXIS2_PLACEMENT_3D('',#17255,#13002,#13003);
#10510=AXIS2_PLACEMENT_3D('',#17257,#13004,#13005);
#10511=AXIS2_PLACEMENT_3D('',#17259,#13006,#13007);
#10512=AXIS2_PLACEMENT_3D('',#17260,#13008,#13009);
#10513=AXIS2_PLACEMENT_3D('',#17261,#13010,#13011);
#10514=AXIS2_PLACEMENT_3D('',#17263,#13012,#13013);
#10515=AXIS2_PLACEMENT_3D('',#17265,#13015,#13016);
#10516=AXIS2_PLACEMENT_3D('',#17267,#13017,#13018);
#10517=AXIS2_PLACEMENT_3D('',#17268,#13019,#13020);
#10518=AXIS2_PLACEMENT_3D('',#17269,#13021,#13022);
#10519=AXIS2_PLACEMENT_3D('',#17272,#13023,#13024);
#10520=AXIS2_PLACEMENT_3D('',#17273,#13025,#13026);
#10521=AXIS2_PLACEMENT_3D('',#17276,#13028,#13029);
#10522=AXIS2_PLACEMENT_3D('',#17277,#13030,#13031);
#10523=AXIS2_PLACEMENT_3D('',#17280,#13033,#13034);
#10524=AXIS2_PLACEMENT_3D('',#17281,#13035,#13036);
#10525=AXIS2_PLACEMENT_3D('',#17291,#13037,#13038);
#10526=AXIS2_PLACEMENT_3D('',#17292,#13039,#13040);
#10527=AXIS2_PLACEMENT_3D('',#17295,#13041,#13042);
#10528=AXIS2_PLACEMENT_3D('',#17297,#13043,#13044);
#10529=AXIS2_PLACEMENT_3D('',#17298,#13045,#13046);
#10530=AXIS2_PLACEMENT_3D('',#17300,#13047,#13048);
#10531=AXIS2_PLACEMENT_3D('',#17301,#13049,#13050);
#10532=AXIS2_PLACEMENT_3D('',#17302,#13051,#13052);
#10533=AXIS2_PLACEMENT_3D('',#17310,#13053,#13054);
#10534=AXIS2_PLACEMENT_3D('',#17318,#13055,#13056);
#10535=AXIS2_PLACEMENT_3D('',#17326,#13057,#13058);
#10536=AXIS2_PLACEMENT_3D('',#17334,#13059,#13060);
#10537=AXIS2_PLACEMENT_3D('',#17342,#13061,#13062);
#10538=AXIS2_PLACEMENT_3D('',#17348,#13066,#13067);
#10539=AXIS2_PLACEMENT_3D('',#17352,#13070,#13071);
#10540=AXIS2_PLACEMENT_3D('',#17356,#13074,#13075);
#10541=AXIS2_PLACEMENT_3D('',#17360,#13078,#13079);
#10542=AXIS2_PLACEMENT_3D('',#17364,#13082,#13083);
#10543=AXIS2_PLACEMENT_3D('',#17366,#13085,#13086);
#10544=AXIS2_PLACEMENT_3D('',#17367,#13087,#13088);
#10545=AXIS2_PLACEMENT_3D('',#17368,#13089,#13090);
#13000=DIRECTION('axis',(0.,0.,1.));
#13001=DIRECTION('refdir',(1.,0.,0.));
#13002=DIRECTION('center_axis',(1.,0.,0.));
#13003=DIRECTION('ref_axis',(0.,0.,-1.));
#13004=DIRECTION('center_axis',(1.,0.,0.));
#13005=DIRECTION('ref_axis',(0.,0.,-1.));
#13006=DIRECTION('center_axis',(0.,1.,1.22464679914735E-16));
#13007=DIRECTION('ref_axis',(0.,-1.22464679914735E-16,1.));
#13008=DIRECTION('center_axis',(1.,0.,0.));
#13009=DIRECTION('ref_axis',(0.,0.,-1.));
#13010=DIRECTION('center_axis',(1.,0.,0.));
#13011=DIRECTION('ref_axis',(0.,0.,-1.));
#13012=DIRECTION('center_axis',(1.,0.,0.));
#13013=DIRECTION('ref_axis',(0.,0.,-1.));
#13014=DIRECTION('',(-1.,0.,0.));
#13015=DIRECTION('center_axis',(1.,0.,0.));
#13016=DIRECTION('ref_axis',(0.,0.,-1.));
#13017=DIRECTION('center_axis',(1.,0.,0.));
#13018=DIRECTION('ref_axis',(0.,0.,-1.));
#13019=DIRECTION('center_axis',(0.,-1.,-1.22464679914735E-16));
#13020=DIRECTION('ref_axis',(0.,-1.22464679914735E-16,1.));
#13021=DIRECTION('center_axis',(1.,0.,0.));
#13022=DIRECTION('ref_axis',(0.,0.,-1.));
#13023=DIRECTION('center_axis',(1.,0.,0.));
#13024=DIRECTION('ref_axis',(0.,0.,-1.));
#13025=DIRECTION('center_axis',(1.,0.,0.));
#13026=DIRECTION('ref_axis',(0.,0.,-1.));
#13027=DIRECTION('',(-1.,0.,0.));
#13028=DIRECTION('center_axis',(1.,0.,0.));
#13029=DIRECTION('ref_axis',(0.,0.,-1.));
#13030=DIRECTION('center_axis',(-1.,0.,0.));
#13031=DIRECTION('ref_axis',(0.,0.,1.));
#13032=DIRECTION('',(0.70710678118655,8.6595605623549E-17,0.707106781186545));
#13033=DIRECTION('center_axis',(1.,0.,0.));
#13034=DIRECTION('ref_axis',(0.,0.,-1.));
#13035=DIRECTION('center_axis',(1.,0.,0.));
#13036=DIRECTION('ref_axis',(0.,0.,-1.));
#13037=DIRECTION('center_axis',(1.,0.,0.));
#13038=DIRECTION('ref_axis',(0.,0.,-1.));
#13039=DIRECTION('center_axis',(1.,0.,0.));
#13040=DIRECTION('ref_axis',(0.,1.,0.));
#13041=DIRECTION('center_axis',(1.,0.,0.));
#13042=DIRECTION('ref_axis',(0.,0.,-1.));
#13043=DIRECTION('center_axis',(1.,0.,0.));
#13044=DIRECTION('ref_axis',(0.,0.,-1.));
#13045=DIRECTION('center_axis',(1.,0.,0.));
#13046=DIRECTION('ref_axis',(0.,0.,-1.));
#13047=DIRECTION('center_axis',(1.,0.,0.));
#13048=DIRECTION('ref_axis',(0.,0.,-1.));
#13049=DIRECTION('center_axis',(1.,0.,0.));
#13050=DIRECTION('ref_axis',(0.,0.,-1.));
#13051=DIRECTION('center_axis',(1.,0.,0.));
#13052=DIRECTION('ref_axis',(0.,0.,-1.));
#13053=DIRECTION('center_axis',(1.,0.,0.));
#13054=DIRECTION('ref_axis',(0.,0.,-1.));
#13055=DIRECTION('center_axis',(1.,0.,0.));
#13056=DIRECTION('ref_axis',(0.,0.,-1.));
#13057=DIRECTION('center_axis',(1.,0.,0.));
#13058=DIRECTION('ref_axis',(0.,0.,-1.));
#13059=DIRECTION('center_axis',(1.,0.,0.));
#13060=DIRECTION('ref_axis',(0.,0.,-1.));
#13061=DIRECTION('center_axis',(0.,0.866025403784439,-0.5));
#13062=DIRECTION('ref_axis',(-1.,0.,0.));
#13063=DIRECTION('',(-1.,0.,0.));
#13064=DIRECTION('',(0.,-0.5,-0.866025403784439));
#13065=DIRECTION('',(-1.,0.,0.));
#13066=DIRECTION('center_axis',(0.,0.866025403784439,0.5));
#13067=DIRECTION('ref_axis',(1.,0.,0.));
#13068=DIRECTION('',(-1.,0.,0.));
#13069=DIRECTION('',(0.,0.5,-0.866025403784439));
#13070=DIRECTION('center_axis',(0.,0.,1.));
#13071=DIRECTION('ref_axis',(1.,0.,0.));
#13072=DIRECTION('',(-1.,0.,0.));
#13073=DIRECTION('',(0.,1.,0.));
#13074=DIRECTION('center_axis',(0.,-0.866025403784439,0.5));
#13075=DIRECTION('ref_axis',(-1.,0.,0.));
#13076=DIRECTION('',(-1.,0.,0.));
#13077=DIRECTION('',(0.,0.5,0.866025403784439));
#13078=DIRECTION('center_axis',(0.,-0.866025403784439,-0.5));
#13079=DIRECTION('ref_axis',(0.,0.5,-0.866025403784439));
#13080=DIRECTION('',(-1.,0.,0.));
#13081=DIRECTION('',(0.,-0.5,0.866025403784439));
#13082=DIRECTION('center_axis',(0.,0.,-1.));
#13083=DIRECTION('ref_axis',(0.,-1.,0.));
#13084=DIRECTION('',(0.,-1.,0.));
#13085=DIRECTION('center_axis',(-1.,0.,0.));
#13086=DIRECTION('ref_axis',(0.,0.,1.));
#13087=DIRECTION('center_axis',(-1.,0.,0.));
#13088=DIRECTION('ref_axis',(0.,0.,1.));
#13089=DIRECTION('center_axis',(-1.,0.,0.));
#13090=DIRECTION('ref_axis',(0.,0.,1.));
#17254=CARTESIAN_POINT('',(0.,0.,0.));
#17255=CARTESIAN_POINT('Origin',(3.556,0.,0.));
#17256=CARTESIAN_POINT('',(3.556,-4.80588143389396E-16,3.9243));
#17257=CARTESIAN_POINT('Origin',(3.556,0.,0.));
#17258=CARTESIAN_POINT('',(3.048,-5.42800200786081E-16,4.4323));
#17259=CARTESIAN_POINT('Origin',(3.556,-5.42800200786081E-16,4.4323));
#17260=CARTESIAN_POINT('Origin',(3.048,0.,0.));
#17261=CARTESIAN_POINT('Origin',(42.926,0.,0.));
#17262=CARTESIAN_POINT('',(32.7025,-4.80588143389396E-16,3.9243));
#17263=CARTESIAN_POINT('Origin',(32.7025,0.,0.));
#17264=CARTESIAN_POINT('',(42.926,-4.80588143389396E-16,3.9243));
#17265=CARTESIAN_POINT('Origin',(32.7025,0.,0.));
#17266=CARTESIAN_POINT('',(33.2105,-4.1837608599271E-16,3.4163));
#17267=CARTESIAN_POINT('Origin',(33.2105,0.,0.));
#17268=CARTESIAN_POINT('Origin',(32.7025,-4.1837608599271E-16,3.4163));
#17269=CARTESIAN_POINT('Origin',(42.926,0.,0.));
#17270=CARTESIAN_POINT('',(41.9354,3.88825358729285E-16,-3.175));
#17271=CARTESIAN_POINT('',(41.9354,-3.88825358729285E-16,3.175));
#17272=CARTESIAN_POINT('Origin',(41.9354,0.,0.));
#17273=CARTESIAN_POINT('Origin',(41.9354,0.,0.));
#17274=CARTESIAN_POINT('',(33.2105,-3.88825358729285E-16,3.175));
#17275=CARTESIAN_POINT('',(42.926,-3.88825358729285E-16,3.175));
#17276=CARTESIAN_POINT('Origin',(33.2105,0.,0.));
#17277=CARTESIAN_POINT('Origin',(41.9354,0.,0.));
#17278=CARTESIAN_POINT('',(42.926,-2.67511846805748E-16,-2.1844));
#17279=CARTESIAN_POINT('',(41.9354,-3.88825358729285E-16,-3.175));
#17280=CARTESIAN_POINT('Origin',(42.926,0.,0.));
#17281=CARTESIAN_POINT('Origin',(0.,0.,0.));
#17282=CARTESIAN_POINT('',(6.97226631718919E-16,-4.83934995634745,2.794));
#17283=CARTESIAN_POINT('',(0.2316331296214,-3.22623330423164,5.588));
#17284=CARTESIAN_POINT('Ctrl Pts',(1.60507362838917E-15,-4.83934995634745,
2.794));
#17285=CARTESIAN_POINT('Ctrl Pts',(1.58206781009085E-15,-4.09069991269487,
4.09069991269492));
#17286=CARTESIAN_POINT('Ctrl Pts',(0.231633129621414,-3.22623330423158,
5.58800000000009));
#17287=CARTESIAN_POINT('',(0.,0.,5.588));
#17288=CARTESIAN_POINT('Ctrl Pts',(0.231633129621415,-3.22623330423175,
5.588));
#17289=CARTESIAN_POINT('Ctrl Pts',(7.23804935274901E-16,-1.49730008730516,
5.588));
#17290=CARTESIAN_POINT('Ctrl Pts',(7.55328766300784E-16,0.,5.588));
#17291=CARTESIAN_POINT('Origin',(0.,0.,0.));
#17292=CARTESIAN_POINT('Origin',(0.,0.,0.));
#17293=CARTESIAN_POINT('',(0.,0.,-5.588));
#17294=CARTESIAN_POINT('',(6.97226631718919E-16,4.83934995634745,-2.794));
#17295=CARTESIAN_POINT('Origin',(0.,0.,0.));
#17296=CARTESIAN_POINT('',(-8.13431070338758E-16,-4.83934995634745,-2.79399999999999));
#17297=CARTESIAN_POINT('Origin',(0.,0.,0.));
#17298=CARTESIAN_POINT('Origin',(0.,0.,0.));
#17299=CARTESIAN_POINT('',(-8.13431070338758E-16,4.83934995634745,2.79399999999999));
#17300=CARTESIAN_POINT('Origin',(0.,0.,0.));
#17301=CARTESIAN_POINT('Origin',(0.,0.,0.));
#17302=CARTESIAN_POINT('Origin',(0.,0.,0.));
#17303=CARTESIAN_POINT('',(0.2316331296214,3.22623330423164,-5.588));
#17304=CARTESIAN_POINT('Ctrl Pts',(1.60507362838917E-15,4.83934995634745,
-2.794));
#17305=CARTESIAN_POINT('Ctrl Pts',(1.58206781009085E-15,4.09069991269487,
-4.09069991269492));
#17306=CARTESIAN_POINT('Ctrl Pts',(0.231633129621414,3.22623330423158,-5.58800000000009));
#17307=CARTESIAN_POINT('Ctrl Pts',(0.231633129621415,3.22623330423175,-5.588));
#17308=CARTESIAN_POINT('Ctrl Pts',(7.23804935274901E-16,1.49730008730516,
-5.588));
#17309=CARTESIAN_POINT('Ctrl Pts',(7.55328766300784E-16,0.,-5.588));
#17310=CARTESIAN_POINT('Origin',(0.,0.,0.));
#17311=CARTESIAN_POINT('',(0.231633129621398,-3.22623330423163,-5.588));
#17312=CARTESIAN_POINT('Ctrl Pts',(7.55328766300784E-16,0.,-5.588));
#17313=CARTESIAN_POINT('Ctrl Pts',(7.49400541621981E-16,-1.49730008730516,
-5.588));
#17314=CARTESIAN_POINT('Ctrl Pts',(0.231633129621414,-3.22623330423174,
-5.588));
#17315=CARTESIAN_POINT('Ctrl Pts',(0.23163312962141,-3.22623330423158,-5.58800000000008));
#17316=CARTESIAN_POINT('Ctrl Pts',(-3.23084588979102E-15,-4.09069991269487,
-4.09069991269491));
#17317=CARTESIAN_POINT('Ctrl Pts',(-2.26598629890234E-15,-4.83934995634745,
-2.79399999999998));
#17318=CARTESIAN_POINT('Origin',(0.,0.,0.));
#17319=CARTESIAN_POINT('',(0.231633129621398,-6.45246660846325,3.02488368589446E-15));
#17320=CARTESIAN_POINT('Ctrl Pts',(-2.26598629890234E-15,-4.83934995634745,
-2.79399999999998));
#17321=CARTESIAN_POINT('Ctrl Pts',(-1.33226762955019E-15,-5.58800000000002,
-1.49730008730506));
#17322=CARTESIAN_POINT('Ctrl Pts',(0.231633129621411,-6.45246660846331,
9.96848220883504E-14));
#17323=CARTESIAN_POINT('Ctrl Pts',(0.231633129621414,-6.45246660846331,
-8.86991478173896E-14));
#17324=CARTESIAN_POINT('Ctrl Pts',(1.66560959941808E-15,-5.58800000000003,
1.49730008730508));
#17325=CARTESIAN_POINT('Ctrl Pts',(1.60507362838917E-15,-4.83934995634745,
2.794));
#17326=CARTESIAN_POINT('Origin',(0.,0.,0.));
#17327=CARTESIAN_POINT('',(0.231633129621398,3.22623330423163,5.588));
#17328=CARTESIAN_POINT('Ctrl Pts',(7.55328766300784E-16,0.,5.588));
#17329=CARTESIAN_POINT('Ctrl Pts',(7.49400541621981E-16,1.49730008730516,
5.588));
#17330=CARTESIAN_POINT('Ctrl Pts',(0.231633129621414,3.22623330423174,5.588));
#17331=CARTESIAN_POINT('Ctrl Pts',(0.23163312962141,3.22623330423158,5.58800000000008));
#17332=CARTESIAN_POINT('Ctrl Pts',(-3.23084588979102E-15,4.09069991269487,
4.09069991269491));
#17333=CARTESIAN_POINT('Ctrl Pts',(-2.26598629890234E-15,4.83934995634745,
2.79399999999998));
#17334=CARTESIAN_POINT('Origin',(0.,0.,0.));
#17335=CARTESIAN_POINT('',(0.231633129621398,6.45246660846325,-3.02488368589446E-15));
#17336=CARTESIAN_POINT('Ctrl Pts',(-2.26598629890234E-15,4.83934995634745,
2.79399999999998));
#17337=CARTESIAN_POINT('Ctrl Pts',(-1.33226762955019E-15,5.58800000000002,
1.49730008730506));
#17338=CARTESIAN_POINT('Ctrl Pts',(0.231633129621411,6.45246660846331,-9.96848220883504E-14));
#17339=CARTESIAN_POINT('Ctrl Pts',(0.231633129621414,6.45246660846331,8.86991478173896E-14));
#17340=CARTESIAN_POINT('Ctrl Pts',(1.66560959941808E-15,5.58800000000003,
-1.49730008730508));
#17341=CARTESIAN_POINT('Ctrl Pts',(1.60507362838917E-15,4.83934995634745,
-2.794));
#17342=CARTESIAN_POINT('Origin',(3.048,-3.22623330423164,5.588));
#17343=CARTESIAN_POINT('',(3.048,-6.45246660846325,0.));
#17344=CARTESIAN_POINT('',(3.048,-6.45246660846325,0.));
#17345=CARTESIAN_POINT('',(3.048,-3.22623330423164,5.588));
#17346=CARTESIAN_POINT('',(3.048,-3.22623330423164,5.588));
#17347=CARTESIAN_POINT('',(3.048,-3.22623330423164,5.588));
#17348=CARTESIAN_POINT('Origin',(3.048,-6.45246660846325,0.));
#17349=CARTESIAN_POINT('',(3.048,-3.22623330423164,-5.588));
#17350=CARTESIAN_POINT('',(3.048,-3.22623330423164,-5.588));
#17351=CARTESIAN_POINT('',(3.048,-6.45246660846325,0.));
#17352=CARTESIAN_POINT('Origin',(3.048,-3.22623330423164,-5.588));
#17353=CARTESIAN_POINT('',(3.048,3.22623330423164,-5.588));
#17354=CARTESIAN_POINT('',(3.048,3.22623330423164,-5.588));
#17355=CARTESIAN_POINT('',(3.048,-3.22623330423164,-5.588));
#17356=CARTESIAN_POINT('Origin',(3.048,3.22623330423164,-5.588));
#17357=CARTESIAN_POINT('',(3.048,6.45246660846325,0.));
#17358=CARTESIAN_POINT('',(3.048,6.45246660846325,0.));
#17359=CARTESIAN_POINT('',(3.048,3.22623330423164,-5.588));
#17360=CARTESIAN_POINT('Origin',(3.048,6.45246660846325,0.));
#17361=CARTESIAN_POINT('',(3.048,3.22623330423164,5.588));
#17362=CARTESIAN_POINT('',(3.048,3.22623330423164,5.588));
#17363=CARTESIAN_POINT('',(3.048,6.45246660846325,0.));
#17364=CARTESIAN_POINT('Origin',(3.048,3.22623330423164,5.588));
#17365=CARTESIAN_POINT('',(3.048,3.22623330423164,5.588));
#17366=CARTESIAN_POINT('Origin',(42.926,2.1844,0.));
#17367=CARTESIAN_POINT('Origin',(33.2105,3.4163,0.));
#17368=CARTESIAN_POINT('Origin',(3.048,6.7056,0.));
#17977=UNCERTAINTY_MEASURE_WITH_UNIT(LENGTH_MEASURE(0.01),#18007,
'DISTANCE_ACCURACY_VALUE',
'Maximum model space distance between geometric entities at asserted c
onnectivities');
#17986=UNCERTAINTY_MEASURE_WITH_UNIT(LENGTH_MEASURE(0.01),#18007,
'DISTANCE_ACCURACY_VALUE',
'Maximum model space distance between geometric entities at asserted c
onnectivities');
#17997=(
GEOMETRIC_REPRESENTATION_CONTEXT(3)
GLOBAL_UNCERTAINTY_ASSIGNED_CONTEXT((#17977))
GLOBAL_UNIT_ASSIGNED_CONTEXT((#18007,#18009,#18010))
REPRESENTATION_CONTEXT('','3D')
);
#18006=(
GEOMETRIC_REPRESENTATION_CONTEXT(3)
GLOBAL_UNCERTAINTY_ASSIGNED_CONTEXT((#17986))
GLOBAL_UNIT_ASSIGNED_CONTEXT((#18007,#18009,#18010))
REPRESENTATION_CONTEXT('','3D')
);
#18007=(
LENGTH_UNIT()
NAMED_UNIT(*)
SI_UNIT(.MILLI.,.METRE.)
);
#18009=(
NAMED_UNIT(*)
PLANE_ANGLE_UNIT()
SI_UNIT($,.RADIAN.)
);
#18010=(
NAMED_UNIT(*)
SI_UNIT($,.STERADIAN.)
SOLID_ANGLE_UNIT()
);
#18021=SHAPE_DEFINITION_REPRESENTATION(#18040,#18080);
#18040=PRODUCT_DEFINITION_SHAPE('',$,#18100);
#18080=SHAPE_REPRESENTATION('',(#10508),#17997);
#18089=PRODUCT_DEFINITION_CONTEXT('part definition',#18148,'design');
#18100=PRODUCT_DEFINITION('Axle Bolt','Axle Bolt',#18119,#18089);
#18119=PRODUCT_DEFINITION_FORMATION('',$,#18160);
#18148=APPLICATION_CONTEXT(
'Core Data for Automotive Mechanical Design Process');
#18149=PRODUCT_CONTEXT('part definition',#18148,'mechanical');
#18160=PRODUCT('Axle Bolt','Axle Bolt',$,(#18149));
#18171=PRESENTATION_STYLE_ASSIGNMENT((#18175));
#18175=SURFACE_STYLE_USAGE(.BOTH.,#18179);
#18179=SURFACE_SIDE_STYLE('',(#18183));
#18183=SURFACE_STYLE_FILL_AREA(#18187);
#18187=FILL_AREA_STYLE('Opaque(61,176,222)',(#18191));
#18191=FILL_AREA_STYLE_COLOUR('Opaque(61,176,222)',#18195);
#18195=COLOUR_RGB('Opaque(61,176,222)',0.23921568627451,0.690196078431373,
0.870588235294118);
ENDSEC;
END-ISO-10303-21;
